ISO-10303-21;
HEADER;
FILE_DESCRIPTION (('STEP AP214'),
    '1' );
FILE_NAME ('rubber 510 pin.step',
    '2026-10-05T20:10:51',
    ( '' ),
    ( '' ),
    'SwSTEP 2.0',
    'SolidWorks 2020',
    '' );
FILE_SCHEMA (( 'AUTOMOTIVE_DESIGN' ));
ENDSEC;

DATA;
#789=CARTESIAN_POINT ( 'NONE',  ( 1.922735082439555487, -0.6236244280033541587, -0.2879360613984097150 ) ) ;
#1493=EDGE_LOOP ( 'NONE', ( #199835, #152427, #123597, #122648, #51346 ) ) ;
#1742=ADVANCED_FACE ( 'NONE', ( #112379 ), #212158, .T. ) ;
#1908=( GEOMETRIC_REPRESENTATION_CONTEXT ( 3 ) GLOBAL_UNCERTAINTY_ASSIGNED_CONTEXT ( ( #209237 ) ) GLOBAL_UNIT_ASSIGNED_CONTEXT ( ( #94356, #65005, #80205 ) ) REPRESENTATION_CONTEXT ( 'NONE', 'WORKASPACE' ) );
#3027=PRESENTATION_STYLE_ASSIGNMENT (( #17146 ) ) ;
#3272=ORIENTED_EDGE ( 'NONE', *, *, #211780, .T. ) ;
#3498=DIRECTION ( 'NONE',  ( 1.000000000000000000, 0.000000000000000000, 0.000000000000000000 ) ) ;
#3714=( GEOMETRIC_REPRESENTATION_CONTEXT ( 3 ) GLOBAL_UNCERTAINTY_ASSIGNED_CONTEXT ( ( #180394 ) ) GLOBAL_UNIT_ASSIGNED_CONTEXT ( ( #122217, #57124, #138389 ) ) REPRESENTATION_CONTEXT ( 'NONE', 'WORKASPACE' ) );
#4093=DIRECTION ( 'NONE',  ( 0.000000000000000000, 0.000000000000000000, 1.000000000000000000 ) ) ;
#5747=FACE_OUTER_BOUND ( 'NONE', #1493, .T. ) ;
#6491=DIRECTION ( 'NONE',  ( 1.224646799147353207E-16, 1.000000000000000000, -0.000000000000000000 ) ) ;
#6687=FILL_AREA_STYLE_COLOUR ( '', #149406 ) ;
#7182=VERTEX_POINT ( 'NONE', #62909 ) ;
#9999=DIRECTION ( 'NONE',  ( -0.000000000000000000, -0.000000000000000000, 1.000000000000000000 ) ) ;
#11760=VERTEX_POINT ( 'NONE', #123031 ) ;
#12262=ORIENTED_EDGE ( 'NONE', *, *, #30664, .T. ) ;
#12338=MECHANICAL_DESIGN_GEOMETRIC_PRESENTATION_REPRESENTATION('',(#88444),#57349);
#13226=AXIS2_PLACEMENT_3D ( 'NONE', #18445, #17366, #83450 ) ;
#13355=CIRCLE ( 'NONE', #47879, 2.021340551328831392 ) ;
#14128=CARTESIAN_POINT ( 'NONE',  ( 0.000000000000000000, 0.000000000000000000, 0.000000000000000000 ) ) ;
#14466=CIRCLE ( 'NONE', #176995, 1.852123800559096534 ) ;
#14715=AXIS2_PLACEMENT_3D ( 'NONE', #15651, #134783, #83860 ) ;
#14789=PRESENTATION_STYLE_ASSIGNMENT (( #126514 ) ) ;
#14911=TOROIDAL_SURFACE ( 'NONE', #70267, 1.821370322827223553, 0.2000000000000000111 ) ;
#15220=( NAMED_UNIT ( * ) PLANE_ANGLE_UNIT ( ) SI_UNIT ( $, .RADIAN. ) );
#15651=CARTESIAN_POINT ( 'NONE',  ( 1.734723475976807094E-15, -3.469446951953614189E-15, 0.2971265334020881110 ) ) ;
#16189=CARTESIAN_POINT ( 'NONE',  ( 0.000000000000000000, 0.000000000000000000, 0.4894596299587841703 ) ) ;
#16274=( LENGTH_UNIT ( ) NAMED_UNIT ( * ) SI_UNIT ( .MILLI., .METRE. ) );
#16581=COLOUR_RGB ( '', 0.72549020, 0.75294118, 0.79215686) ;
#16738=( GEOMETRIC_REPRESENTATION_CONTEXT ( 3 ) GLOBAL_UNCERTAINTY_ASSIGNED_CONTEXT ( ( #20359 ) ) GLOBAL_UNIT_ASSIGNED_CONTEXT ( ( #16274, #15220, #184119 ) ) REPRESENTATION_CONTEXT ( 'NONE', 'WORKASPACE' ) );
#16861=EDGE_CURVE ( 'NONE', #84638, #18660, #116530, .T. ) ;
#17146=SURFACE_STYLE_USAGE ( .BOTH. , #119008 ) ;
#17366=DIRECTION ( 'NONE',  ( 0.000000000000000000, 0.000000000000000000, 1.000000000000000000 ) ) ;
#17618=FILL_AREA_STYLE ('',( #169228 ) ) ;
#18445=CARTESIAN_POINT ( 'NONE',  ( 0.000000000000000000, 0.000000000000000000, -6.123233995736775897E-17 ) ) ;
#18660=VERTEX_POINT ( 'NONE', #111278 ) ;
#19291=DIRECTION ( 'NONE',  ( 1.000000000000000000, 0.000000000000000000, 0.000000000000000000 ) ) ;
#19482=DIRECTION ( 'NONE',  ( 0.000000000000000000, 0.000000000000000000, -1.000000000000000000 ) ) ;
#19539=CARTESIAN_POINT ( 'NONE',  ( 0.000000000000000000, 0.000000000000000000, -0.4856446947087145194 ) ) ;
#20292=DIRECTION ( 'NONE',  ( -1.000000000000000000, 4.440892098500626162E-15, 0.000000000000000000 ) ) ;
#20359=UNCERTAINTY_MEASURE_WITH_UNIT (LENGTH_MEASURE( 1.000000000000000082E-05 ), #16274, 'distance_accuracy_value', 'NONE');
#20725=FILL_AREA_STYLE_COLOUR ( '', #146345 ) ;
#21023=ADVANCED_FACE ( 'NONE', ( #66953 ), #200157, .T. ) ;
#22022=AXIS2_PLACEMENT_3D ( 'NONE', #99968, #67428, #3498 ) ;
#23697=ORIENTED_EDGE ( 'NONE', *, *, #192598, .T. ) ;
#23748=STYLED_ITEM ( 'NONE', ( #3027 ), #21023 ) ;
#23966=EDGE_LOOP ( 'NONE', ( #82571, #100656, #100077, #36916 ) ) ;
#26330=DIRECTION ( 'NONE',  ( -1.000000000000000000, 0.000000000000000000, 0.000000000000000000 ) ) ;
#26746=( LENGTH_UNIT ( ) NAMED_UNIT ( * ) SI_UNIT ( .MILLI., .METRE. ) );
#27182=CARTESIAN_POINT ( 'NONE',  ( 0.000000000000000000, 0.000000000000000000, -6.123233995736775897E-17 ) ) ;
#28208=FILL_AREA_STYLE_COLOUR ( '', #71333 ) ;
#28447=CARTESIAN_POINT ( 'NONE',  ( -1.749999999999999778, 2.143131898507868051E-16, 0.000000000000000000 ) ) ;
#28720=STYLED_ITEM ( 'NONE', ( #73991 ), #81823 ) ;
#28976=AXIS2_PLACEMENT_3D ( 'NONE', #194619, #176258, #30002 ) ;
#29348=DIRECTION ( 'NONE',  ( 0.000000000000000000, 0.000000000000000000, 1.000000000000000000 ) ) ;
#29904=ORIENTED_EDGE ( 'NONE', *, *, #181023, .F. ) ;
#30002=DIRECTION ( 'NONE',  ( 1.000000000000000000, 0.000000000000000000, 0.000000000000000000 ) ) ;
#30304=AXIS2_PLACEMENT_3D ( 'NONE', #74433, #39797, #121132 ) ;
#30410=SURFACE_STYLE_USAGE ( .BOTH. , #179850 ) ;
#30581=ORIENTED_EDGE ( 'NONE', *, *, #101820, .F. ) ;
#30664=EDGE_CURVE ( 'NONE', #79740, #161718, #104776, .T. ) ;
#30737=MECHANICAL_DESIGN_GEOMETRIC_PRESENTATION_REPRESENTATION('',(#23748),#120780);
#31454=MECHANICAL_DESIGN_GEOMETRIC_PRESENTATION_REPRESENTATION('',(#145589),#58955);
#32223=CARTESIAN_POINT ( 'NONE',  ( -1.749999999999999778, 2.143131898507868051E-16, 0.000000000000000000 ) ) ;
#32370=MECHANICAL_DESIGN_GEOMETRIC_PRESENTATION_REPRESENTATION('',(#139542),#91154);
#32633=EDGE_CURVE ( 'NONE', #151743, #109340, #142994, .T. ) ;
#32700=DIRECTION ( 'NONE',  ( 0.000000000000000000, -1.000000000000000000, 0.000000000000000000 ) ) ;
#32933=AXIS2_PLACEMENT_3D ( 'NONE', #32223, #66809, #162234 ) ;
#33418=FILL_AREA_STYLE_COLOUR ( '', #151805 ) ;
#33557=DIRECTION ( 'NONE',  ( -0.000000000000000000, -1.000000000000000000, -0.000000000000000000 ) ) ;
#33890=SURFACE_SIDE_STYLE ('',( #136744 ) ) ;
#34222=AXIS2_PLACEMENT_3D ( 'NONE', #210784, #192392, #146890 ) ;
#34642=PRESENTATION_STYLE_ASSIGNMENT (( #117029 ) ) ;
#36019=FACE_OUTER_BOUND ( 'NONE', #172557, .T. ) ;
#36246=CARTESIAN_POINT ( 'NONE',  ( 1.249999999999998890, 0.000000000000000000, -6.123233995736774664E-17 ) ) ;
#36563=AXIS2_PLACEMENT_3D ( 'NONE', #137896, #9999, #104318 ) ;
#36810=ADVANCED_FACE ( 'NONE', ( #209134 ), #99911, .T. ) ;
#36916=ORIENTED_EDGE ( 'NONE', *, *, #144311, .T. ) ;
#37021=EDGE_LOOP ( 'NONE', ( #113052, #180091, #192697, #169705 ) ) ;
#37478=MECHANICAL_DESIGN_GEOMETRIC_PRESENTATION_REPRESENTATION('',(#137691),#16738);
#37696=( LENGTH_UNIT ( ) NAMED_UNIT ( * ) SI_UNIT ( .MILLI., .METRE. ) );
#37743=COLOUR_RGB ( '', 0.09019608, 0.27058824, 0.51372549) ;
#39140=( NAMED_UNIT ( * ) SI_UNIT ( $, .STERADIAN. ) SOLID_ANGLE_UNIT ( ) );
#39797=DIRECTION ( 'NONE',  ( -0.000000000000000000, -0.000000000000000000, 1.000000000000000000 ) ) ;
#41216=CIRCLE ( 'NONE', #34222, 0.2000000000000000944 ) ;
#41371=( NAMED_UNIT ( * ) SI_UNIT ( $, .STERADIAN. ) SOLID_ANGLE_UNIT ( ) );
#42438=PRESENTATION_STYLE_ASSIGNMENT (( #189719 ) ) ;
#42585=( NAMED_UNIT ( * ) PLANE_ANGLE_UNIT ( ) SI_UNIT ( $, .RADIAN. ) );
#43470=COLOUR_RGB ( '', 0.66274510, 0.83137255, 0.94901961) ;
#44421=EDGE_CURVE ( 'NONE', #161718, #204270, #68492, .T. ) ;
#44659=EDGE_CURVE ( 'NONE', #134155, #204270, #161923, .T. ) ;
#45612=FILL_AREA_STYLE ('',( #196116 ) ) ;
#45836=CARTESIAN_POINT ( 'NONE',  ( 1.734723475976807094E-15, -3.469446951953614189E-15, 0.2971265334020881110 ) ) ;
#46201=STYLED_ITEM ( 'NONE', ( #52285 ), #114026 ) ;
#46741=CARTESIAN_POINT ( 'NONE',  ( 2.011244508837064071, -3.469446951953614189E-15, 0.2971265334020881110 ) ) ;
#47171=ORIENTED_EDGE ( 'NONE', *, *, #52529, .F. ) ;
#47879=AXIS2_PLACEMENT_3D ( 'NONE', #103704, #149238, #20292 ) ;
#48906=DIRECTION ( 'NONE',  ( 0.000000000000000000, 0.000000000000000000, -1.000000000000000000 ) ) ;
#48997=EDGE_CURVE ( 'NONE', #59844, #161718, #170121, .T. ) ;
#49851=ADVANCED_FACE ( 'NONE', ( #138862 ), #211700, .T. ) ;
#50793=( GEOMETRIC_REPRESENTATION_CONTEXT ( 3 ) GLOBAL_UNCERTAINTY_ASSIGNED_CONTEXT ( ( #87799 ) ) GLOBAL_UNIT_ASSIGNED_CONTEXT ( ( #61778, #161422, #205502 ) ) REPRESENTATION_CONTEXT ( 'NONE', 'WORKASPACE' ) );
#51346=ORIENTED_EDGE ( 'NONE', *, *, #144311, .F. ) ;
#51975=( NAMED_UNIT ( * ) PLANE_ANGLE_UNIT ( ) SI_UNIT ( $, .RADIAN. ) );
#52285=PRESENTATION_STYLE_ASSIGNMENT (( #150866 ) ) ;
#52529=EDGE_CURVE ( 'NONE', #109340, #84638, #208451, .T. ) ;
#53253=SURFACE_STYLE_FILL_AREA ( #186437 ) ;
#53664=UNCERTAINTY_MEASURE_WITH_UNIT (LENGTH_MEASURE( 1.000000000000000082E-05 ), #37696, 'distance_accuracy_value', 'NONE');
#53802=ADVANCED_FACE ( 'NONE', ( #69476 ), #205044, .T. ) ;
#53902=AXIS2_PLACEMENT_3D ( 'NONE', #210039, #144043, #172515 ) ;
#55259=ORIENTED_EDGE ( 'NONE', *, *, #123827, .F. ) ;
#55269=CARTESIAN_POINT ( 'NONE',  ( -1.811274280335455122, -3.247629826974540057E-15, 0.2936757779752607878 ) ) ;
#56393=( GEOMETRIC_REPRESENTATION_CONTEXT ( 3 ) GLOBAL_UNCERTAINTY_ASSIGNED_CONTEXT ( ( #188434 ) ) GLOBAL_UNIT_ASSIGNED_CONTEXT ( ( #137934, #42585, #71824 ) ) REPRESENTATION_CONTEXT ( 'NONE', 'WORKASPACE' ) );
#56532=SURFACE_STYLE_FILL_AREA ( #72763 ) ;
#56772=EDGE_CURVE ( 'NONE', #85578, #59844, #177711, .T. ) ;
#56920=ORIENTED_EDGE ( 'NONE', *, *, #32633, .T. ) ;
#57124=( NAMED_UNIT ( * ) PLANE_ANGLE_UNIT ( ) SI_UNIT ( $, .RADIAN. ) );
#57349=( GEOMETRIC_REPRESENTATION_CONTEXT ( 3 ) GLOBAL_UNCERTAINTY_ASSIGNED_CONTEXT ( ( #106179 ) ) GLOBAL_UNIT_ASSIGNED_CONTEXT ( ( #134317, #51975, #114900 ) ) REPRESENTATION_CONTEXT ( 'NONE', 'WORKASPACE' ) );
#57598=( NAMED_UNIT ( * ) PLANE_ANGLE_UNIT ( ) SI_UNIT ( $, .RADIAN. ) );
#57678=CIRCLE ( 'NONE', #178749, 1.868950538045371035 ) ;
#58690=ORIENTED_EDGE ( 'NONE', *, *, #203936, .T. ) ;
#58743=CARTESIAN_POINT ( 'NONE',  ( -1.852123800559039468, 2.268197483979258082E-16, 0.4894596299587841703 ) ) ;
#58955=( GEOMETRIC_REPRESENTATION_CONTEXT ( 3 ) GLOBAL_UNCERTAINTY_ASSIGNED_CONTEXT ( ( #98100 ) ) GLOBAL_UNIT_ASSIGNED_CONTEXT ( ( #26746, #105919, #73355 ) ) REPRESENTATION_CONTEXT ( 'NONE', 'WORKASPACE' ) );
#59844=VERTEX_POINT ( 'NONE', #177580 ) ;
#60697=COLOUR_RGB ( '', 0.72549020, 0.75294118, 0.79215686) ;
#60998=DIRECTION ( 'NONE',  ( -1.000000000000000000, 0.000000000000000000, 0.000000000000000000 ) ) ;
#61778=( LENGTH_UNIT ( ) NAMED_UNIT ( * ) SI_UNIT ( .MILLI., .METRE. ) );
#61831=DIRECTION ( 'NONE',  ( 0.000000000000000000, 0.000000000000000000, 1.000000000000000000 ) ) ;
#61880=ORIENTED_EDGE ( 'NONE', *, *, #48997, .F. ) ;
#62909=CARTESIAN_POINT ( 'NONE',  ( 2.021340551328831836, -3.221904128336454264E-15, -0.2879360613984097150 ) ) ;
#63448=COLOUR_RGB ( '', 0.66274510, 0.83137255, 0.94901961) ;
#63817=AXIS2_PLACEMENT_3D ( 'NONE', #177483, #141826, #206764 ) ;
#63992=PRESENTATION_STYLE_ASSIGNMENT (( #65035 ) ) ;
#64465=EDGE_CURVE ( 'NONE', #11760, #134155, #94389, .T. ) ;
#64625=SURFACE_SIDE_STYLE ('',( #145914 ) ) ;
#65005=( NAMED_UNIT ( * ) PLANE_ANGLE_UNIT ( ) SI_UNIT ( $, .RADIAN. ) );
#65035=SURFACE_STYLE_USAGE ( .BOTH. , #162572 ) ;
#66174=UNCERTAINTY_MEASURE_WITH_UNIT (LENGTH_MEASURE( 1.000000000000000082E-05 ), #132509, 'distance_accuracy_value', 'NONE');
#66809=DIRECTION ( 'NONE',  ( 1.224646799147353207E-16, 1.000000000000000000, -0.000000000000000000 ) ) ;
#66953=FACE_OUTER_BOUND ( 'NONE', #157997, .T. ) ;
#67391=ORIENTED_EDGE ( 'NONE', *, *, #16861, .T. ) ;
#67428=DIRECTION ( 'NONE',  ( 0.000000000000000000, 0.000000000000000000, 1.000000000000000000 ) ) ;
#67498=ORIENTED_EDGE ( 'NONE', *, *, #64465, .F. ) ;
#67735=PRODUCT_CONTEXT ( 'NONE', #181919, 'mechanical' ) ;
#68020=FILL_AREA_STYLE ('',( #33418 ) ) ;
#68077=AXIS2_PLACEMENT_3D ( 'NONE', #55269, #6491, #72566 ) ;
#68492=CIRCLE ( 'NONE', #175840, 0.5000000000000007772 ) ;
#68725=AXIS2_PLACEMENT_3D ( 'NONE', #135219, #4093, #19291 ) ;
#69476=FACE_OUTER_BOUND ( 'NONE', #179566, .T. ) ;
#69753=STYLED_ITEM ( 'NONE', ( #42438 ), #49851 ) ;
#70267=AXIS2_PLACEMENT_3D ( 'NONE', #108690, #172566, #123899 ) ;
#70633=( NAMED_UNIT ( * ) SI_UNIT ( $, .STERADIAN. ) SOLID_ANGLE_UNIT ( ) );
#71119=DIRECTION ( 'NONE',  ( 1.000000000000000000, 0.000000000000000000, 0.000000000000000000 ) ) ;
#71333=COLOUR_RGB ( '', 0.66274510, 0.83137255, 0.94901961) ;
#71824=( NAMED_UNIT ( * ) SI_UNIT ( $, .STERADIAN. ) SOLID_ANGLE_UNIT ( ) );
#72280=PRESENTATION_STYLE_ASSIGNMENT (( #157839 ) ) ;
#72557=DIRECTION ( 'NONE',  ( -0.000000000000000000, -0.000000000000000000, -1.000000000000000000 ) ) ;
#72566=DIRECTION ( 'NONE',  ( -1.000000000000000000, 1.224646799147347537E-16, 0.000000000000000000 ) ) ;
#72763=FILL_AREA_STYLE ('',( #6687 ) ) ;
#73355=( NAMED_UNIT ( * ) SI_UNIT ( $, .STERADIAN. ) SOLID_ANGLE_UNIT ( ) );
#73991=PRESENTATION_STYLE_ASSIGNMENT (( #106541 ) ) ;
#73997=DIRECTION ( 'NONE',  ( 1.224646799147353207E-16, 1.000000000000000000, -0.000000000000000000 ) ) ;
#74368=CIRCLE ( 'NONE', #32933, 0.5000000000000008882 ) ;
#74433=CARTESIAN_POINT ( 'NONE',  ( 1.734723475976807094E-15, -3.469446951953614189E-15, -0.2879360613984097150 ) ) ;
#74775=EDGE_CURVE ( 'NONE', #85578, #79740, #14466, .T. ) ;
#74869=ORIENTED_EDGE ( 'NONE', *, *, #74775, .T. ) ;
#75978=SURFACE_SIDE_STYLE ('',( #56532 ) ) ;
#76996=DIRECTION ( 'NONE',  ( 0.000000000000000000, 0.000000000000000000, 1.000000000000000000 ) ) ;
#77672=FILL_AREA_STYLE ('',( #164261 ) ) ;
#78910=CIRCLE ( 'NONE', #13226, 1.249999999999998890 ) ;
#79740=VERTEX_POINT ( 'NONE', #181915 ) ;
#80205=( NAMED_UNIT ( * ) SI_UNIT ( $, .STERADIAN. ) SOLID_ANGLE_UNIT ( ) );
#80220=( NAMED_UNIT ( * ) PLANE_ANGLE_UNIT ( ) SI_UNIT ( $, .RADIAN. ) );
#81277=PRESENTATION_STYLE_ASSIGNMENT (( #30410 ) ) ;
#81823=ADVANCED_FACE ( 'NONE', ( #5747 ), #14911, .T. ) ;
#82011=ORIENTED_EDGE ( 'NONE', *, *, #56772, .F. ) ;
#82046=CIRCLE ( 'NONE', #140866, 0.2000000000000000111 ) ;
#82483=VECTOR ( 'NONE', #204727, 1000.000000000000114 ) ;
#82571=ORIENTED_EDGE ( 'NONE', *, *, #87621, .F. ) ;
#82606=CARTESIAN_POINT ( 'NONE',  ( -1.868950538045364596, 2.288804294181979298E-16, -0.4856446947087145194 ) ) ;
#83070=ORIENTED_EDGE ( 'NONE', *, *, #52529, .T. ) ;
#83450=DIRECTION ( 'NONE',  ( 1.000000000000000000, 0.000000000000000000, 0.000000000000000000 ) ) ;
#83860=DIRECTION ( 'NONE',  ( -1.000000000000000000, 0.000000000000000000, 0.000000000000000000 ) ) ;
#84638=VERTEX_POINT ( 'NONE', #46741 ) ;
#85325=CARTESIAN_POINT ( 'NONE',  ( -1.902435570468859805, 0.6170404364503311312, 0.9487424039605132364 ) ) ;
#85521=ORIENTED_EDGE ( 'NONE', *, *, #87621, .T. ) ;
#85578=VERTEX_POINT ( 'NONE', #58743 ) ;
#85671=LINE ( 'NONE', #200468, #82483 ) ;
#85752=SURFACE_STYLE_USAGE ( .BOTH. , #202676 ) ;
#86820=CARTESIAN_POINT ( 'NONE',  ( 1.734723475976807094E-15, -3.469446951953614189E-15, 0.2936757779752607878 ) ) ;
#87621=EDGE_CURVE ( 'NONE', #59844, #134155, #74368, .T. ) ;
#87799=UNCERTAINTY_MEASURE_WITH_UNIT (LENGTH_MEASURE( 1.000000000000000082E-05 ), #61778, 'distance_accuracy_value', 'NONE');
#88387=AXIS2_PLACEMENT_3D ( 'NONE', #131157, #61831, #197148 ) ;
#88444=STYLED_ITEM ( 'NONE', ( #34642 ), #88722 ) ;
#88722=MANIFOLD_SOLID_BREP ( 'Fillet1', #136432 ) ;
#90037=DIRECTION ( 'NONE',  ( 0.000000000000000000, 0.000000000000000000, 1.000000000000000000 ) ) ;
#91154=( GEOMETRIC_REPRESENTATION_CONTEXT ( 3 ) GLOBAL_UNCERTAINTY_ASSIGNED_CONTEXT ( ( #114474 ) ) GLOBAL_UNIT_ASSIGNED_CONTEXT ( ( #130764, #143792, #127592 ) ) REPRESENTATION_CONTEXT ( 'NONE', 'WORKASPACE' ) );
#91331=SURFACE_SIDE_STYLE ('',( #169352 ) ) ;
#92412=DIRECTION ( 'NONE',  ( -1.000000000000000000, 1.224646799147352714E-16, 0.000000000000000000 ) ) ;
#93069=CARTESIAN_POINT ( 'NONE',  ( 1.734723475976807094E-15, -3.469446951953614189E-15, -0.2879360613984097150 ) ) ;
#93615=COLOUR_RGB ( '', 0.66274510, 0.83137255, 0.94901961) ;
#94302=SURFACE_SIDE_STYLE ('',( #110595 ) ) ;
#94356=( LENGTH_UNIT ( ) NAMED_UNIT ( * ) SI_UNIT ( .MILLI., .METRE. ) );
#94385=FILL_AREA_STYLE ('',( #178827 ) ) ;
#94389=CIRCLE ( 'NONE', #115297, 0.1999999999999999833 ) ;
#94585=AXIS2_PLACEMENT_3D ( 'NONE', #135843, #106587, #206156 ) ;
#95216=CARTESIAN_POINT ( 'NONE',  ( 0.000000000000000000, 0.000000000000000000, 0.000000000000000000 ) ) ;
#95372=FILL_AREA_STYLE ('',( #28208 ) ) ;
#95443=SURFACE_SIDE_STYLE ('',( #111727 ) ) ;
#97254=ORIENTED_EDGE ( 'NONE', *, *, #127848, .T. ) ;
#97260=EDGE_LOOP ( 'NONE', ( #119416, #135212, #127701, #67498, #123164 ) ) ;
#97545=SURFACE_SIDE_STYLE ('',( #199257 ) ) ;
#97580=CARTESIAN_POINT ( 'NONE',  ( 1.734723475976807094E-15, -3.469446951953614189E-15, 0.9487424039605132364 ) ) ;
#97688=ORIENTED_EDGE ( 'NONE', *, *, #101820, .T. ) ;
#98100=UNCERTAINTY_MEASURE_WITH_UNIT (LENGTH_MEASURE( 1.000000000000000082E-05 ), #26746, 'distance_accuracy_value', 'NONE');
#98541=DIRECTION ( 'NONE',  ( -0.000000000000000000, -0.000000000000000000, 1.000000000000000000 ) ) ;
#98612=PRESENTATION_STYLE_ASSIGNMENT (( #164673 ) ) ;
#98782=DIRECTION ( 'NONE',  ( 0.000000000000000000, 0.000000000000000000, -1.000000000000000000 ) ) ;
#99652=FILL_AREA_STYLE_COLOUR ( '', #43470 ) ;
#99840=DIRECTION ( 'NONE',  ( -0.000000000000000000, -0.000000000000000000, -1.000000000000000000 ) ) ;
#99911=TOROIDAL_SURFACE ( 'NONE', #134247, 1.749999999999999778, 0.5000000000000007772 ) ;
#99968=CARTESIAN_POINT ( 'NONE',  ( 0.000000000000000000, 0.000000000000000000, 0.000000000000000000 ) ) ;
#100077=ORIENTED_EDGE ( 'NONE', *, *, #44421, .T. ) ;
#100656=ORIENTED_EDGE ( 'NONE', *, *, #48997, .T. ) ;
#101820=EDGE_CURVE ( 'NONE', #84638, #79740, #82046, .T. ) ;
#103019=ORIENTED_EDGE ( 'NONE', *, *, #74775, .F. ) ;
#103704=CARTESIAN_POINT ( 'NONE',  ( 1.734723475976807094E-15, -3.469446951953614189E-15, -0.2879360613984097150 ) ) ;
#104318=DIRECTION ( 'NONE',  ( -1.000000000000000000, 0.000000000000000000, 0.000000000000000000 ) ) ;
#104776=CIRCLE ( 'NONE', #146379, 0.5000000000000007772 ) ;
#105894=CARTESIAN_POINT ( 'NONE',  ( 1.868950538045364596, 0.000000000000000000, -0.4856446947087145194 ) ) ;
#105919=( NAMED_UNIT ( * ) PLANE_ANGLE_UNIT ( ) SI_UNIT ( $, .RADIAN. ) );
#106179=UNCERTAINTY_MEASURE_WITH_UNIT (LENGTH_MEASURE( 1.000000000000000082E-05 ), #134317, 'distance_accuracy_value', 'NONE');
#106541=SURFACE_STYLE_USAGE ( .BOTH. , #91331 ) ;
#106587=DIRECTION ( 'NONE',  ( 0.000000000000000000, 0.000000000000000000, -1.000000000000000000 ) ) ;
#108690=CARTESIAN_POINT ( 'NONE',  ( 1.734723475976807094E-15, -3.469446951953614189E-15, -0.2913868168252300994 ) ) ;
#108884=CIRCLE ( 'NONE', #63817, 2.011244508837062295 ) ;
#109340=VERTEX_POINT ( 'NONE', #197840 ) ;
#109636=AXIS2_PLACEMENT_3D ( 'NONE', #138399, #188189, #204418 ) ;
#109820=DIRECTION ( 'NONE',  ( 0.000000000000000000, 0.000000000000000000, -1.000000000000000000 ) ) ;
#110595=SURFACE_STYLE_FILL_AREA ( #95372 ) ;
#111278=CARTESIAN_POINT ( 'NONE',  ( 1.913131547260902510, -0.6205095947705829840, 0.2971265334020881110 ) ) ;
#111400=EDGE_CURVE ( 'NONE', #117810, #11760, #170482, .T. ) ;
#111716=SURFACE_STYLE_FILL_AREA ( #210195 ) ;
#111727=SURFACE_STYLE_FILL_AREA ( #45612 ) ;
#111752=AXIS2_PLACEMENT_3D ( 'NONE', #86820, #90037, #152885 ) ;
#112379=FACE_OUTER_BOUND ( 'NONE', #198219, .T. ) ;
#112813=FACE_OUTER_BOUND ( 'NONE', #113847, .T. ) ;
#113052=ORIENTED_EDGE ( 'NONE', *, *, #202198, .F. ) ;
#113847=EDGE_LOOP ( 'NONE', ( #129209, #209937, #56920, #58690, #117637, #155235 ) ) ;
#113855=FILL_AREA_STYLE_COLOUR ( '', #60697 ) ;
#114026=ADVANCED_FACE ( 'NONE', ( #36019 ), #191497, .T. ) ;
#114474=UNCERTAINTY_MEASURE_WITH_UNIT (LENGTH_MEASURE( 1.000000000000000082E-05 ), #130764, 'distance_accuracy_value', 'NONE');
#114900=( NAMED_UNIT ( * ) SI_UNIT ( $, .STERADIAN. ) SOLID_ANGLE_UNIT ( ) );
#115297=AXIS2_PLACEMENT_3D ( 'NONE', #149445, #33557, #183001 ) ;
#115500=( GEOMETRIC_REPRESENTATION_CONTEXT ( 3 ) GLOBAL_UNCERTAINTY_ASSIGNED_CONTEXT ( ( #66174 ) ) GLOBAL_UNIT_ASSIGNED_CONTEXT ( ( #132509, #120562, #70633 ) ) REPRESENTATION_CONTEXT ( 'NONE', 'WORKASPACE' ) );
#115676=ORIENTED_EDGE ( 'NONE', *, *, #127848, .F. ) ;
#115980=ORIENTED_EDGE ( 'NONE', *, *, #204649, .T. ) ;
#116530=CIRCLE ( 'NONE', #168420, 2.011244508837062295 ) ;
#116862=( NAMED_UNIT ( * ) PLANE_ANGLE_UNIT ( ) SI_UNIT ( $, .RADIAN. ) );
#117029=SURFACE_STYLE_USAGE ( .BOTH. , #97545 ) ;
#117113=EDGE_LOOP ( 'NONE', ( #83070, #67391, #115980, #3272, #23697, #117599 ) ) ;
#117599=ORIENTED_EDGE ( 'NONE', *, *, #203936, .F. ) ;
#117637=ORIENTED_EDGE ( 'NONE', *, *, #111400, .T. ) ;
#117810=VERTEX_POINT ( 'NONE', #150846 ) ;
#118316=PRESENTATION_STYLE_ASSIGNMENT (( #85752 ) ) ;
#119008=SURFACE_SIDE_STYLE ('',( #133092 ) ) ;
#119416=ORIENTED_EDGE ( 'NONE', *, *, #192598, .F. ) ;
#120427=DIRECTION ( 'NONE',  ( 1.000000000000000000, 0.000000000000000000, 0.000000000000000000 ) ) ;
#120562=( NAMED_UNIT ( * ) PLANE_ANGLE_UNIT ( ) SI_UNIT ( $, .RADIAN. ) );
#120780=( GEOMETRIC_REPRESENTATION_CONTEXT ( 3 ) GLOBAL_UNCERTAINTY_ASSIGNED_CONTEXT ( ( #53664 ) ) GLOBAL_UNIT_ASSIGNED_CONTEXT ( ( #37696, #116862, #182864 ) ) REPRESENTATION_CONTEXT ( 'NONE', 'WORKASPACE' ) );
#120838=STYLED_ITEM ( 'NONE', ( #98612 ), #36810 ) ;
#121132=DIRECTION ( 'NONE',  ( -1.000000000000000000, 0.000000000000000000, 0.000000000000000000 ) ) ;
#121890=ADVANCED_FACE ( 'NONE', ( #148419 ), #181734, .T. ) ;
#122217=( LENGTH_UNIT ( ) NAMED_UNIT ( * ) SI_UNIT ( .MILLI., .METRE. ) );
#122648=ORIENTED_EDGE ( 'NONE', *, *, #64465, .T. ) ;
#123031=CARTESIAN_POINT ( 'NONE',  ( -2.021340551328828283, -3.469446951953614189E-15, -0.2879360613984097150 ) ) ;
#123164=ORIENTED_EDGE ( 'NONE', *, *, #111400, .F. ) ;
#123597=ORIENTED_EDGE ( 'NONE', *, *, #146492, .F. ) ;
#123827=EDGE_CURVE ( 'NONE', #79740, #85578, #130054, .T. ) ;
#123899=DIRECTION ( 'NONE',  ( -1.000000000000000000, 0.000000000000000000, 0.000000000000000000 ) ) ;
#124347=SHAPE_REPRESENTATION_RELATIONSHIP ( 'NONE' , 'NONE' ,  #141543, #184056 ) ;
#124734=CARTESIAN_POINT ( 'NONE',  ( -2.011244508837060518, -3.223140536948614282E-15, 0.2971265334020881110 ) ) ;
#125222=( GEOMETRIC_REPRESENTATION_CONTEXT ( 3 ) GLOBAL_UNCERTAINTY_ASSIGNED_CONTEXT ( ( #194583 ) ) GLOBAL_UNIT_ASSIGNED_CONTEXT ( ( #156177, #57598, #41371 ) ) REPRESENTATION_CONTEXT ( 'NONE', 'WORKASPACE' ) );
#125527=STYLED_ITEM ( 'NONE', ( #118316 ), #53802 ) ;
#126462=ADVANCED_FACE ( 'NONE', ( #162488 ), #182210, .T. ) ;
#126514=SURFACE_STYLE_USAGE ( .BOTH. , #64625 ) ;
#126667=APPLICATION_CONTEXT ( 'automotive_design' ) ;
#127592=( NAMED_UNIT ( * ) SI_UNIT ( $, .STERADIAN. ) SOLID_ANGLE_UNIT ( ) );
#127701=ORIENTED_EDGE ( 'NONE', *, *, #44659, .F. ) ;
#127848=EDGE_CURVE ( 'NONE', #151743, #85578, #161522, .T. ) ;
#128644=PRODUCT_DEFINITION ( 'UNKNOWN', '', #173395, #184634 ) ;
#129209=ORIENTED_EDGE ( 'NONE', *, *, #204649, .F. ) ;
#130054=CIRCLE ( 'NONE', #36563, 1.852123800559096534 ) ;
#130764=( LENGTH_UNIT ( ) NAMED_UNIT ( * ) SI_UNIT ( .MILLI., .METRE. ) );
#131157=CARTESIAN_POINT ( 'NONE',  ( 0.000000000000000000, 0.000000000000000000, 0.000000000000000000 ) ) ;
#131765=UNCERTAINTY_MEASURE_WITH_UNIT (LENGTH_MEASURE( 1.000000000000000082E-05 ), #160410, 'distance_accuracy_value', 'NONE');
#132002=DIRECTION ( 'NONE',  ( 0.000000000000000000, 0.000000000000000000, 1.000000000000000000 ) ) ;
#132509=( LENGTH_UNIT ( ) NAMED_UNIT ( * ) SI_UNIT ( .MILLI., .METRE. ) );
#133092=SURFACE_STYLE_FILL_AREA ( #68020 ) ;
#133252=FILL_AREA_STYLE ('',( #99652 ) ) ;
#133366=PRODUCT_DEFINITION_SHAPE ( 'NONE', 'NONE',  #128644 ) ;
#134155=VERTEX_POINT ( 'NONE', #82606 ) ;
#134247=AXIS2_PLACEMENT_3D ( 'NONE', #14128, #29348, #161493 ) ;
#134317=( LENGTH_UNIT ( ) NAMED_UNIT ( * ) SI_UNIT ( .MILLI., .METRE. ) );
#134783=DIRECTION ( 'NONE',  ( 0.000000000000000000, 0.000000000000000000, -1.000000000000000000 ) ) ;
#135212=ORIENTED_EDGE ( 'NONE', *, *, #213029, .T. ) ;
#135219=CARTESIAN_POINT ( 'NONE',  ( 1.734723475976807094E-15, -3.469446951953614189E-15, 0.2936757779752607878 ) ) ;
#135396=DIRECTION ( 'NONE',  ( -0.9512177852344306794, 0.3085202182251672864, 0.000000000000000000 ) ) ;
#135797=FILL_AREA_STYLE ('',( #202892 ) ) ;
#135843=CARTESIAN_POINT ( 'NONE',  ( 1.734723475976807094E-15, -3.469446951953614189E-15, 0.2971265334020881110 ) ) ;
#135987=SHAPE_DEFINITION_REPRESENTATION ( #133366, #141543 ) ;
#136432=CLOSED_SHELL ( 'NONE', ( #36810, #1742, #126462, #53802, #49851, #121890, #114026, #210444, #21023, #81823 ) ) ;
#136651=( NAMED_UNIT ( * ) PLANE_ANGLE_UNIT ( ) SI_UNIT ( $, .RADIAN. ) );
#136744=SURFACE_STYLE_FILL_AREA ( #17618 ) ;
#137691=STYLED_ITEM ( 'NONE', ( #63992 ), #210444 ) ;
#137844=CONICAL_SURFACE ( 'NONE', #193174, 2.000000000000000000, 0.01725463330310792257 ) ;
#137896=CARTESIAN_POINT ( 'NONE',  ( 0.000000000000000000, 0.000000000000000000, 0.4894596299587841703 ) ) ;
#137934=( LENGTH_UNIT ( ) NAMED_UNIT ( * ) SI_UNIT ( .MILLI., .METRE. ) );
#138389=( NAMED_UNIT ( * ) SI_UNIT ( $, .STERADIAN. ) SOLID_ANGLE_UNIT ( ) );
#138399=CARTESIAN_POINT ( 'NONE',  ( 1.734723475976807094E-15, -3.469446951953614189E-15, -0.2913868168252300994 ) ) ;
#138785=( LENGTH_UNIT ( ) NAMED_UNIT ( * ) SI_UNIT ( .MILLI., .METRE. ) );
#138862=FACE_OUTER_BOUND ( 'NONE', #117113, .T. ) ;
#139368=( GEOMETRIC_REPRESENTATION_CONTEXT ( 3 ) GLOBAL_UNCERTAINTY_ASSIGNED_CONTEXT ( ( #170606 ) ) GLOBAL_UNIT_ASSIGNED_CONTEXT ( ( #138785, #136651, #39140 ) ) REPRESENTATION_CONTEXT ( 'NONE', 'WORKASPACE' ) );
#139458=SURFACE_STYLE_FILL_AREA ( #141617 ) ;
#139542=STYLED_ITEM ( 'NONE', ( #14789 ), #1742 ) ;
#140866=AXIS2_PLACEMENT_3D ( 'NONE', #212443, #182071, #48906 ) ;
#141543=SHAPE_REPRESENTATION ( 'rubber 510 pin', ( #200407 ), #3714 ) ;
#141617=FILL_AREA_STYLE ('',( #187109 ) ) ;
#141826=DIRECTION ( 'NONE',  ( 0.000000000000000000, 0.000000000000000000, -1.000000000000000000 ) ) ;
#142081=CARTESIAN_POINT ( 'NONE',  ( 1.734723475976807094E-15, -3.469446951953614189E-15, 0.9487424039605132364 ) ) ;
#142293=ORIENTED_EDGE ( 'NONE', *, *, #44659, .T. ) ;
#142994=CIRCLE ( 'NONE', #94585, 2.011244508837062295 ) ;
#143792=( NAMED_UNIT ( * ) PLANE_ANGLE_UNIT ( ) SI_UNIT ( $, .RADIAN. ) );
#144043=DIRECTION ( 'NONE',  ( -0.000000000000000000, -0.000000000000000000, 1.000000000000000000 ) ) ;
#144143=PRESENTATION_STYLE_ASSIGNMENT (( #160343 ) ) ;
#144311=EDGE_CURVE ( 'NONE', #204270, #134155, #57678, .T. ) ;
#145589=STYLED_ITEM ( 'NONE', ( #72280 ), #184056 ) ;
#145914=SURFACE_STYLE_FILL_AREA ( #77672 ) ;
#146026=MECHANICAL_DESIGN_GEOMETRIC_PRESENTATION_REPRESENTATION('',(#69753),#125222);
#146345=COLOUR_RGB ( '', 0.66274510, 0.83137255, 0.94901961) ;
#146379=AXIS2_PLACEMENT_3D ( 'NONE', #192363, #155623, #209679 ) ;
#146492=EDGE_CURVE ( 'NONE', #11760, #188370, #157871, .T. ) ;
#146890=DIRECTION ( 'NONE',  ( -1.000000000000000000, -1.224646799147346058E-16, 0.000000000000000000 ) ) ;
#148419=FACE_OUTER_BOUND ( 'NONE', #37021, .T. ) ;
#148458=MECHANICAL_DESIGN_GEOMETRIC_PRESENTATION_REPRESENTATION('',(#120838),#193292);
#148594=CARTESIAN_POINT ( 'NONE',  ( 1.749999999999999778, 0.000000000000000000, 0.000000000000000000 ) ) ;
#149238=DIRECTION ( 'NONE',  ( -0.000000000000000000, -0.000000000000000000, 1.000000000000000000 ) ) ;
#149406=COLOUR_RGB ( '', 0.40784314, 0.44705882, 0.49803922) ;
#149445=CARTESIAN_POINT ( 'NONE',  ( -1.821370322827221777, -3.469446951953614189E-15, -0.2913868168252300994 ) ) ;
#150846=CARTESIAN_POINT ( 'NONE',  ( -1.922735082439551935, 0.6236244280033473864, -0.2879360613984097150 ) ) ;
#150866=SURFACE_STYLE_USAGE ( .BOTH. , #33890 ) ;
#151743=VERTEX_POINT ( 'NONE', #124734 ) ;
#151805=COLOUR_RGB ( '', 0.72549020, 0.75294118, 0.79215686) ;
#152427=ORIENTED_EDGE ( 'NONE', *, *, #211780, .F. ) ;
#152885=DIRECTION ( 'NONE',  ( 1.000000000000000000, 0.000000000000000000, 0.000000000000000000 ) ) ;
#154608=DIRECTION ( 'NONE',  ( -0.01641209967245726292, 0.005323139086630728802, -0.9998511425080263137 ) ) ;
#155235=ORIENTED_EDGE ( 'NONE', *, *, #146492, .T. ) ;
#155623=DIRECTION ( 'NONE',  ( 0.000000000000000000, -1.000000000000000000, 0.000000000000000000 ) ) ;
#156177=( LENGTH_UNIT ( ) NAMED_UNIT ( * ) SI_UNIT ( .MILLI., .METRE. ) );
#156380=AXIS2_PLACEMENT_3D ( 'NONE', #27182, #76996, #71119 ) ;
#156998=DIRECTION ( 'NONE',  ( -0.000000000000000000, -0.000000000000000000, 1.000000000000000000 ) ) ;
#157839=SURFACE_STYLE_USAGE ( .BOTH. , #189254 ) ;
#157871=CIRCLE ( 'NONE', #30304, 2.021340551328831392 ) ;
#157997=EDGE_LOOP ( 'NONE', ( #115676, #29904, #164897, #97688, #103019 ) ) ;
#160343=SURFACE_STYLE_USAGE ( .BOTH. , #94302 ) ;
#160410=( LENGTH_UNIT ( ) NAMED_UNIT ( * ) SI_UNIT ( .MILLI., .METRE. ) );
#161199=CIRCLE ( 'NONE', #53902, 2.021340551328831392 ) ;
#161266=DIRECTION ( 'NONE',  ( 1.000000000000000000, 0.000000000000000000, 0.000000000000000000 ) ) ;
#161422=( NAMED_UNIT ( * ) PLANE_ANGLE_UNIT ( ) SI_UNIT ( $, .RADIAN. ) );
#161493=DIRECTION ( 'NONE',  ( 1.000000000000000000, 0.000000000000000000, 0.000000000000000000 ) ) ;
#161522=CIRCLE ( 'NONE', #68077, 0.1999999999999998723 ) ;
#161718=VERTEX_POINT ( 'NONE', #36246 ) ;
#161923=CIRCLE ( 'NONE', #182610, 1.868950538045371035 ) ;
#162234=DIRECTION ( 'NONE',  ( -1.000000000000000000, 1.224646799147352714E-16, 0.000000000000000000 ) ) ;
#162488=FACE_OUTER_BOUND ( 'NONE', #97260, .T. ) ;
#162572=SURFACE_SIDE_STYLE ('',( #212352 ) ) ;
#163862=MECHANICAL_DESIGN_GEOMETRIC_PRESENTATION_REPRESENTATION('',(#46201),#115500);
#164261=FILL_AREA_STYLE_COLOUR ( '', #63448 ) ;
#164440=STYLED_ITEM ( 'NONE', ( #81277 ), #121890 ) ;
#164673=SURFACE_STYLE_USAGE ( .BOTH. , #95443 ) ;
#164897=ORIENTED_EDGE ( 'NONE', *, *, #16861, .F. ) ;
#167043=MECHANICAL_DESIGN_GEOMETRIC_PRESENTATION_REPRESENTATION('',(#125527),#139368);
#168158=STYLED_ITEM ( 'NONE', ( #144143 ), #126462 ) ;
#168420=AXIS2_PLACEMENT_3D ( 'NONE', #45836, #109820, #60998 ) ;
#169228=FILL_AREA_STYLE_COLOUR ( '', #170789 ) ;
#169352=SURFACE_STYLE_FILL_AREA ( #135797 ) ;
#169705=ORIENTED_EDGE ( 'NONE', *, *, #56772, .T. ) ;
#170121=CIRCLE ( 'NONE', #156380, 1.249999999999998890 ) ;
#170482=CIRCLE ( 'NONE', #187648, 2.021340551328831392 ) ;
#170606=UNCERTAINTY_MEASURE_WITH_UNIT (LENGTH_MEASURE( 1.000000000000000082E-05 ), #138785, 'distance_accuracy_value', 'NONE');
#170789=COLOUR_RGB ( '', 0.08235294, 0.09019608, 0.10196078) ;
#172515=DIRECTION ( 'NONE',  ( -1.000000000000000000, 0.000000000000000000, 0.000000000000000000 ) ) ;
#172557=EDGE_LOOP ( 'NONE', ( #61880, #82011, #74869, #12262 ) ) ;
#172566=DIRECTION ( 'NONE',  ( 0.000000000000000000, 0.000000000000000000, -1.000000000000000000 ) ) ;
#173395=PRODUCT_DEFINITION_FORMATION_WITH_SPECIFIED_SOURCE ( 'ANY', '', #199001, .NOT_KNOWN. ) ;
#173566=AXIS2_PLACEMENT_3D ( 'NONE', #142081, #208096, #204879 ) ;
#174321=DIRECTION ( 'NONE',  ( -1.000000000000000000, -2.664535259100375697E-15, 0.000000000000000000 ) ) ;
#175840=AXIS2_PLACEMENT_3D ( 'NONE', #148594, #32700, #98782 ) ;
#176138=ORIENTED_EDGE ( 'NONE', *, *, #44421, .F. ) ;
#176258=DIRECTION ( 'NONE',  ( 0.000000000000000000, 0.000000000000000000, 1.000000000000000000 ) ) ;
#176995=AXIS2_PLACEMENT_3D ( 'NONE', #16189, #98541, #26330 ) ;
#177483=CARTESIAN_POINT ( 'NONE',  ( 1.734723475976807094E-15, -3.469446951953614189E-15, 0.2971265334020881110 ) ) ;
#177580=CARTESIAN_POINT ( 'NONE',  ( -1.249999999999998890, 1.530808498934190585E-16, -6.123233995736774664E-17 ) ) ;
#177711=CIRCLE ( 'NONE', #205351, 0.5000000000000008882 ) ;
#178749=AXIS2_PLACEMENT_3D ( 'NONE', #19539, #72557, #204677 ) ;
#178806=( NAMED_UNIT ( * ) SI_UNIT ( $, .STERADIAN. ) SOLID_ANGLE_UNIT ( ) );
#178827=FILL_AREA_STYLE_COLOUR ( '', #16581 ) ;
#179566=EDGE_LOOP ( 'NONE', ( #184978, #97254, #55259, #30581, #47171 ) ) ;
#179850=SURFACE_SIDE_STYLE ('',( #111716 ) ) ;
#180091=ORIENTED_EDGE ( 'NONE', *, *, #30664, .F. ) ;
#180394=UNCERTAINTY_MEASURE_WITH_UNIT (LENGTH_MEASURE( 1.000000000000000082E-05 ), #122217, 'distance_accuracy_value', 'NONE');
#180995=COLOUR_RGB ( '', 0.40784314, 0.44705882, 0.49803922) ;
#181023=EDGE_CURVE ( 'NONE', #18660, #151743, #108884, .T. ) ;
#181734=TOROIDAL_SURFACE ( 'NONE', #88387, 1.749999999999999778, 0.5000000000000007772 ) ;
#181915=CARTESIAN_POINT ( 'NONE',  ( 1.852123800559039468, 0.000000000000000000, 0.4894596299587841703 ) ) ;
#181919=APPLICATION_CONTEXT ( 'automotive_design' ) ;
#182071=DIRECTION ( 'NONE',  ( 0.000000000000000000, -1.000000000000000000, 0.000000000000000000 ) ) ;
#182132=CARTESIAN_POINT ( 'NONE',  ( 0.000000000000000000, 0.000000000000000000, -0.4856446947087145194 ) ) ;
#182210=TOROIDAL_SURFACE ( 'NONE', #109636, 1.821370322827223553, 0.2000000000000000111 ) ;
#182610=AXIS2_PLACEMENT_3D ( 'NONE', #182132, #99840, #120427 ) ;
#182864=( NAMED_UNIT ( * ) SI_UNIT ( $, .STERADIAN. ) SOLID_ANGLE_UNIT ( ) );
#183001=DIRECTION ( 'NONE',  ( 0.000000000000000000, 0.000000000000000000, -1.000000000000000000 ) ) ;
#184056=ADVANCED_BREP_SHAPE_REPRESENTATION ( '', ( #88722, #200407 ), #3714 ) ;
#184119=( NAMED_UNIT ( * ) SI_UNIT ( $, .STERADIAN. ) SOLID_ANGLE_UNIT ( ) );
#184634=PRODUCT_DEFINITION_CONTEXT ( 'detailed design', #126667, 'design' ) ;
#184978=ORIENTED_EDGE ( 'NONE', *, *, #32633, .F. ) ;
#185139=MECHANICAL_DESIGN_GEOMETRIC_PRESENTATION_REPRESENTATION('',(#164440),#1908);
#186437=FILL_AREA_STYLE ('',( #20725 ) ) ;
#186667=ORIENTED_EDGE ( 'NONE', *, *, #202198, .T. ) ;
#187086=LINE ( 'NONE', #85325, #196599 ) ;
#187109=FILL_AREA_STYLE_COLOUR ( '', #93615 ) ;
#187648=AXIS2_PLACEMENT_3D ( 'NONE', #93069, #156998, #174321 ) ;
#188189=DIRECTION ( 'NONE',  ( 0.000000000000000000, 0.000000000000000000, -1.000000000000000000 ) ) ;
#188370=VERTEX_POINT ( 'NONE', #789 ) ;
#188434=UNCERTAINTY_MEASURE_WITH_UNIT (LENGTH_MEASURE( 1.000000000000000082E-05 ), #137934, 'distance_accuracy_value', 'NONE');
#189254=SURFACE_SIDE_STYLE ('',( #139458 ) ) ;
#189719=SURFACE_STYLE_USAGE ( .BOTH. , #75978 ) ;
#191497=TOROIDAL_SURFACE ( 'NONE', #22022, 1.749999999999999778, 0.5000000000000007772 ) ;
#192363=CARTESIAN_POINT ( 'NONE',  ( 1.749999999999999778, 0.000000000000000000, 0.000000000000000000 ) ) ;
#192392=DIRECTION ( 'NONE',  ( -1.224646799147353207E-16, 1.000000000000000000, 0.000000000000000000 ) ) ;
#192598=EDGE_CURVE ( 'NONE', #7182, #117810, #161199, .T. ) ;
#192697=ORIENTED_EDGE ( 'NONE', *, *, #123827, .T. ) ;
#193174=AXIS2_PLACEMENT_3D ( 'NONE', #97580, #19482, #135396 ) ;
#193292=( GEOMETRIC_REPRESENTATION_CONTEXT ( 3 ) GLOBAL_UNCERTAINTY_ASSIGNED_CONTEXT ( ( #131765 ) ) GLOBAL_UNIT_ASSIGNED_CONTEXT ( ( #160410, #80220, #178806 ) ) REPRESENTATION_CONTEXT ( 'NONE', 'WORKASPACE' ) );
#194583=UNCERTAINTY_MEASURE_WITH_UNIT (LENGTH_MEASURE( 1.000000000000000082E-05 ), #156177, 'distance_accuracy_value', 'NONE');
#194619=CARTESIAN_POINT ( 'NONE',  ( 0.000000000000000000, 0.000000000000000000, 0.000000000000000000 ) ) ;
#196116=FILL_AREA_STYLE_COLOUR ( '', #37743 ) ;
#196599=VECTOR ( 'NONE', #154608, 1000.000000000000114 ) ;
#197148=DIRECTION ( 'NONE',  ( 1.000000000000000000, 0.000000000000000000, 0.000000000000000000 ) ) ;
#197840=CARTESIAN_POINT ( 'NONE',  ( -1.913131547260899179, 0.6205095947705763226, 0.2971265334020881110 ) ) ;
#198219=EDGE_LOOP ( 'NONE', ( #176138, #186667, #85521, #142293 ) ) ;
#199001=PRODUCT ( 'rubber 510 pin', 'rubber 510 pin', '', ( #67735 ) ) ;
#199257=SURFACE_STYLE_FILL_AREA ( #133252 ) ;
#199835=ORIENTED_EDGE ( 'NONE', *, *, #213029, .F. ) ;
#200157=TOROIDAL_SURFACE ( 'NONE', #68725, 1.811274280335456677, 0.2000000000000000111 ) ;
#200407=AXIS2_PLACEMENT_3D ( 'NONE', #95216, #132002, #161266 ) ;
#200468=CARTESIAN_POINT ( 'NONE',  ( 1.902435570468863135, -0.6170404364503377925, 0.9487424039605132364 ) ) ;
#202198=EDGE_CURVE ( 'NONE', #161718, #59844, #78910, .T. ) ;
#202676=SURFACE_SIDE_STYLE ('',( #53253 ) ) ;
#202892=FILL_AREA_STYLE_COLOUR ( '', #180995 ) ;
#203936=EDGE_CURVE ( 'NONE', #109340, #117810, #187086, .T. ) ;
#204270=VERTEX_POINT ( 'NONE', #105894 ) ;
#204418=DIRECTION ( 'NONE',  ( -1.000000000000000000, 0.000000000000000000, 0.000000000000000000 ) ) ;
#204649=EDGE_CURVE ( 'NONE', #18660, #188370, #85671, .T. ) ;
#204677=DIRECTION ( 'NONE',  ( 1.000000000000000000, 0.000000000000000000, 0.000000000000000000 ) ) ;
#204727=DIRECTION ( 'NONE',  ( 0.01641209967245726292, -0.005323139086630727067, -0.9998511425080263137 ) ) ;
#204879=DIRECTION ( 'NONE',  ( -0.9512177852344306794, 0.3085202182251672864, 0.000000000000000000 ) ) ;
#205044=TOROIDAL_SURFACE ( 'NONE', #111752, 1.811274280335456677, 0.2000000000000000111 ) ;
#205100=MECHANICAL_DESIGN_GEOMETRIC_PRESENTATION_REPRESENTATION('',(#28720),#56393);
#205351=AXIS2_PLACEMENT_3D ( 'NONE', #28447, #73997, #92412 ) ;
#205502=( NAMED_UNIT ( * ) SI_UNIT ( $, .STERADIAN. ) SOLID_ANGLE_UNIT ( ) );
#206156=DIRECTION ( 'NONE',  ( -1.000000000000000000, 0.000000000000000000, 0.000000000000000000 ) ) ;
#206764=DIRECTION ( 'NONE',  ( -1.000000000000000000, 0.000000000000000000, 0.000000000000000000 ) ) ;
#208096=DIRECTION ( 'NONE',  ( 0.000000000000000000, 0.000000000000000000, -1.000000000000000000 ) ) ;
#208451=CIRCLE ( 'NONE', #14715, 2.011244508837062295 ) ;
#209134=FACE_OUTER_BOUND ( 'NONE', #23966, .T. ) ;
#209237=UNCERTAINTY_MEASURE_WITH_UNIT (LENGTH_MEASURE( 1.000000000000000082E-05 ), #94356, 'distance_accuracy_value', 'NONE');
#209679=DIRECTION ( 'NONE',  ( 0.000000000000000000, 0.000000000000000000, -1.000000000000000000 ) ) ;
#209723=MECHANICAL_DESIGN_GEOMETRIC_PRESENTATION_REPRESENTATION('',(#168158),#50793);
#209937=ORIENTED_EDGE ( 'NONE', *, *, #181023, .T. ) ;
#210039=CARTESIAN_POINT ( 'NONE',  ( 1.734723475976807094E-15, -3.469446951953614189E-15, -0.2879360613984097150 ) ) ;
#210195=FILL_AREA_STYLE ('',( #113855 ) ) ;
#210444=ADVANCED_FACE ( 'NONE', ( #112813 ), #137844, .T. ) ;
#210784=CARTESIAN_POINT ( 'NONE',  ( 1.821370322827225330, -3.246393418362380038E-15, -0.2913868168252300994 ) ) ;
#211700=CONICAL_SURFACE ( 'NONE', #173566, 2.000000000000000000, 0.01725463330310792257 ) ;
#211780=EDGE_CURVE ( 'NONE', #188370, #7182, #13355, .T. ) ;
#212158=TOROIDAL_SURFACE ( 'NONE', #28976, 1.749999999999999778, 0.5000000000000007772 ) ;
#212352=SURFACE_STYLE_FILL_AREA ( #94385 ) ;
#212443=CARTESIAN_POINT ( 'NONE',  ( 1.811274280335458453, -3.469446951953614189E-15, 0.2936757779752607878 ) ) ;
#213029=EDGE_CURVE ( 'NONE', #7182, #204270, #41216, .T. ) ;
ENDSEC;
END-ISO-10303-21;
